ISO-10303-21;
HEADER;
/* Generated by software containing ST-Developer
 * from STEP Tools, Inc. (www.steptools.com) 
 */

FILE_DESCRIPTION(
/* description */ ('Worm-less right-angle friction wheel drive'),
/* implementation_level */ '2;1');

FILE_NAME(
/* name */ 'Cap Screw - M5x20.step',
/* time_stamp */ '2026-10-28T03:22:36-07:00',
/* author */ (''),
/* organization */ (''),
/* preprocessor_version */ 'ST-DEVELOPER v20.2',
/* originating_system */ 'Autodesk Translation Framework v15.17.0.0',
/* authorisation */ '');

FILE_SCHEMA (('AUTOMOTIVE_DESIGN { 1 0 10303 214 3 1 1 }'));
ENDSEC;

DATA;
#10=MECHANICAL_DESIGN_GEOMETRIC_PRESENTATION_REPRESENTATION('',(#634),#17046);
#451=ORIENTED_CLOSED_SHELL('',*,#8190,.F.);
#455=CONICAL_SURFACE('',#9238,0.4,0.785398163397448);
#456=CONICAL_SURFACE('',#9242,0.41,0.785398163397448);
#457=CONICAL_SURFACE('',#9246,0.26,0.463647609000806);
#458=CONICAL_SURFACE('',#9250,0.225,0.785398163397448);
#477=BREP_WITH_VOIDS('Body1',#8189,(#451));
#540=SHAPE_REPRESENTATION_RELATIONSHIP('SRR','None',#17283,#587);
#587=ADVANCED_BREP_SHAPE_REPRESENTATION('',(#477),#17019);
#634=STYLED_ITEM('',(#17598),#477);
#905=FACE_BOUND('',#2103,.T.);
#1068=PLANE('',#9236);
#1069=PLANE('',#9244);
#1070=PLANE('',#9252);
#1071=PLANE('',#9253);
#1072=PLANE('',#9254);
#1073=PLANE('',#9255);
#1074=PLANE('',#9256);
#1075=PLANE('',#9257);
#1076=PLANE('',#9258);
#1077=PLANE('',#9259);
#1078=PLANE('',#9260);
#1442=FACE_OUTER_BOUND('',#2098,.T.);
#1443=FACE_OUTER_BOUND('',#2099,.T.);
#1444=FACE_OUTER_BOUND('',#2100,.T.);
#1445=FACE_OUTER_BOUND('',#2101,.T.);
#1446=FACE_OUTER_BOUND('',#2102,.T.);
#1447=FACE_OUTER_BOUND('',#2104,.T.);
#1448=FACE_OUTER_BOUND('',#2105,.T.);
#1449=FACE_OUTER_BOUND('',#2106,.T.);
#1450=FACE_OUTER_BOUND('',#2107,.T.);
#1451=FACE_OUTER_BOUND('',#2108,.T.);
#1452=FACE_OUTER_BOUND('',#2109,.T.);
#1453=FACE_OUTER_BOUND('',#2110,.T.);
#1454=FACE_OUTER_BOUND('',#2111,.T.);
#1455=FACE_OUTER_BOUND('',#2112,.T.);
#1456=FACE_OUTER_BOUND('',#2113,.T.);
#1457=FACE_OUTER_BOUND('',#2114,.T.);
#1458=FACE_OUTER_BOUND('',#2115,.T.);
#2098=EDGE_LOOP('',(#6602));
#2099=EDGE_LOOP('',(#6603,#6604,#6605,#6606));
#2100=EDGE_LOOP('',(#6607,#6608,#6609,#6610));
#2101=EDGE_LOOP('',(#6611,#6612,#6613,#6614));
#2102=EDGE_LOOP('',(#6615));
#2103=EDGE_LOOP('',(#6616));
#2104=EDGE_LOOP('',(#6617,#6618,#6619,#6620));
#2105=EDGE_LOOP('',(#6621,#6622,#6623,#6624));
#2106=EDGE_LOOP('',(#6625,#6626,#6627,#6628));
#2107=EDGE_LOOP('',(#6629));
#2108=EDGE_LOOP('',(#6630,#6631,#6632,#6633));
#2109=EDGE_LOOP('',(#6634,#6635,#6636,#6637));
#2110=EDGE_LOOP('',(#6638,#6639,#6640,#6641));
#2111=EDGE_LOOP('',(#6642,#6643,#6644,#6645));
#2112=EDGE_LOOP('',(#6646,#6647,#6648,#6649));
#2113=EDGE_LOOP('',(#6650,#6651,#6652,#6653));
#2114=EDGE_LOOP('',(#6654,#6655,#6656,#6657,#6658,#6659));
#2115=EDGE_LOOP('',(#6660,#6661,#6662,#6663,#6664,#6665));
#2673=LINE('',#15331,#3213);
#2674=LINE('',#15335,#3214);
#2675=LINE('',#15339,#3215);
#2676=LINE('',#15346,#3216);
#2677=LINE('',#15350,#3217);
#2678=LINE('',#15354,#3218);
#2679=LINE('',#15359,#3219);
#2680=LINE('',#15361,#3220);
#2681=LINE('',#15363,#3221);
#2682=LINE('',#15364,#3222);
#2683=LINE('',#15367,#3223);
#2684=LINE('',#15369,#3224);
#2685=LINE('',#15370,#3225);
#2686=LINE('',#15373,#3226);
#2687=LINE('',#15375,#3227);
#2688=LINE('',#15376,#3228);
#2689=LINE('',#15379,#3229);
#2690=LINE('',#15381,#3230);
#2691=LINE('',#15382,#3231);
#2692=LINE('',#15385,#3232);
#2693=LINE('',#15387,#3233);
#2694=LINE('',#15388,#3234);
#2695=LINE('',#15390,#3235);
#2696=LINE('',#15391,#3236);
#3213=VECTOR('',#11065,0.4);
#3214=VECTOR('',#11070,0.425);
#3215=VECTOR('',#11075,0.41);
#3216=VECTOR('',#11084,0.26);
#3217=VECTOR('',#11089,0.25);
#3218=VECTOR('',#11094,0.225);
#3219=VECTOR('',#11099,1.);
#3220=VECTOR('',#11100,1.);
#3221=VECTOR('',#11101,1.);
#3222=VECTOR('',#11102,1.);
#3223=VECTOR('',#11105,1.);
#3224=VECTOR('',#11106,1.);
#3225=VECTOR('',#11107,1.);
#3226=VECTOR('',#11110,1.);
#3227=VECTOR('',#11111,1.);
#3228=VECTOR('',#11112,1.);
#3229=VECTOR('',#11115,1.);
#3230=VECTOR('',#11116,1.);
#3231=VECTOR('',#11117,1.);
#3232=VECTOR('',#11120,1.);
#3233=VECTOR('',#11121,1.);
#3234=VECTOR('',#11122,1.);
#3235=VECTOR('',#11125,1.);
#3236=VECTOR('',#11126,1.);
#3693=CIRCLE('',#9237,0.375);
#3694=CIRCLE('',#9239,0.425);
#3695=CIRCLE('',#9241,0.425);
#3696=CIRCLE('',#9243,0.395);
#3697=CIRCLE('',#9245,0.27);
#3698=CIRCLE('',#9247,0.24505);
#3699=CIRCLE('',#9249,0.24505);
#3700=CIRCLE('',#9251,0.2);
#4225=VERTEX_POINT('',#15326);
#4226=VERTEX_POINT('',#15329);
#4227=VERTEX_POINT('',#15333);
#4228=VERTEX_POINT('',#15337);
#4229=VERTEX_POINT('',#15341);
#4230=VERTEX_POINT('',#15344);
#4231=VERTEX_POINT('',#15348);
#4232=VERTEX_POINT('',#15352);
#4233=VERTEX_POINT('',#15357);
#4234=VERTEX_POINT('',#15358);
#4235=VERTEX_POINT('',#15360);
#4236=VERTEX_POINT('',#15362);
#4237=VERTEX_POINT('',#15366);
#4238=VERTEX_POINT('',#15368);
#4239=VERTEX_POINT('',#15372);
#4240=VERTEX_POINT('',#15374);
#4241=VERTEX_POINT('',#15378);
#4242=VERTEX_POINT('',#15380);
#4243=VERTEX_POINT('',#15384);
#4244=VERTEX_POINT('',#15386);
#5070=EDGE_CURVE('',#4225,#4225,#3693,.T.);
#5071=EDGE_CURVE('',#4226,#4226,#3694,.T.);
#5072=EDGE_CURVE('',#4226,#4225,#2673,.T.);
#5073=EDGE_CURVE('',#4227,#4227,#3695,.T.);
#5074=EDGE_CURVE('',#4227,#4226,#2674,.T.);
#5075=EDGE_CURVE('',#4228,#4228,#3696,.T.);
#5076=EDGE_CURVE('',#4228,#4227,#2675,.T.);
#5077=EDGE_CURVE('',#4229,#4229,#3697,.T.);
#5078=EDGE_CURVE('',#4230,#4230,#3698,.F.);
#5079=EDGE_CURVE('',#4230,#4229,#2676,.T.);
#5080=EDGE_CURVE('',#4231,#4231,#3699,.F.);
#5081=EDGE_CURVE('',#4231,#4230,#2677,.T.);
#5082=EDGE_CURVE('',#4232,#4232,#3700,.T.);
#5083=EDGE_CURVE('',#4232,#4231,#2678,.T.);
#5084=EDGE_CURVE('',#4233,#4234,#2679,.T.);
#5085=EDGE_CURVE('',#4234,#4235,#2680,.T.);
#5086=EDGE_CURVE('',#4235,#4236,#2681,.T.);
#5087=EDGE_CURVE('',#4233,#4236,#2682,.T.);
#5088=EDGE_CURVE('',#4234,#4237,#2683,.T.);
#5089=EDGE_CURVE('',#4237,#4238,#2684,.T.);
#5090=EDGE_CURVE('',#4238,#4235,#2685,.T.);
#5091=EDGE_CURVE('',#4237,#4239,#2686,.T.);
#5092=EDGE_CURVE('',#4239,#4240,#2687,.T.);
#5093=EDGE_CURVE('',#4240,#4238,#2688,.T.);
#5094=EDGE_CURVE('',#4239,#4241,#2689,.T.);
#5095=EDGE_CURVE('',#4241,#4242,#2690,.T.);
#5096=EDGE_CURVE('',#4242,#4240,#2691,.T.);
#5097=EDGE_CURVE('',#4241,#4243,#2692,.T.);
#5098=EDGE_CURVE('',#4243,#4244,#2693,.T.);
#5099=EDGE_CURVE('',#4244,#4242,#2694,.T.);
#5100=EDGE_CURVE('',#4243,#4233,#2695,.T.);
#5101=EDGE_CURVE('',#4236,#4244,#2696,.T.);
#6602=ORIENTED_EDGE('',*,*,#5070,.F.);
#6603=ORIENTED_EDGE('',*,*,#5071,.F.);
#6604=ORIENTED_EDGE('',*,*,#5072,.T.);
#6605=ORIENTED_EDGE('',*,*,#5070,.T.);
#6606=ORIENTED_EDGE('',*,*,#5072,.F.);
#6607=ORIENTED_EDGE('',*,*,#5073,.F.);
#6608=ORIENTED_EDGE('',*,*,#5074,.T.);
#6609=ORIENTED_EDGE('',*,*,#5071,.T.);
#6610=ORIENTED_EDGE('',*,*,#5074,.F.);
#6611=ORIENTED_EDGE('',*,*,#5075,.F.);
#6612=ORIENTED_EDGE('',*,*,#5076,.T.);
#6613=ORIENTED_EDGE('',*,*,#5073,.T.);
#6614=ORIENTED_EDGE('',*,*,#5076,.F.);
#6615=ORIENTED_EDGE('',*,*,#5075,.T.);
#6616=ORIENTED_EDGE('',*,*,#5077,.F.);
#6617=ORIENTED_EDGE('',*,*,#5078,.F.);
#6618=ORIENTED_EDGE('',*,*,#5079,.T.);
#6619=ORIENTED_EDGE('',*,*,#5077,.T.);
#6620=ORIENTED_EDGE('',*,*,#5079,.F.);
#6621=ORIENTED_EDGE('',*,*,#5080,.F.);
#6622=ORIENTED_EDGE('',*,*,#5081,.T.);
#6623=ORIENTED_EDGE('',*,*,#5078,.T.);
#6624=ORIENTED_EDGE('',*,*,#5081,.F.);
#6625=ORIENTED_EDGE('',*,*,#5082,.F.);
#6626=ORIENTED_EDGE('',*,*,#5083,.T.);
#6627=ORIENTED_EDGE('',*,*,#5080,.T.);
#6628=ORIENTED_EDGE('',*,*,#5083,.F.);
#6629=ORIENTED_EDGE('',*,*,#5082,.T.);
#6630=ORIENTED_EDGE('',*,*,#5084,.T.);
#6631=ORIENTED_EDGE('',*,*,#5085,.T.);
#6632=ORIENTED_EDGE('',*,*,#5086,.T.);
#6633=ORIENTED_EDGE('',*,*,#5087,.F.);
#6634=ORIENTED_EDGE('',*,*,#5088,.T.);
#6635=ORIENTED_EDGE('',*,*,#5089,.T.);
#6636=ORIENTED_EDGE('',*,*,#5090,.T.);
#6637=ORIENTED_EDGE('',*,*,#5085,.F.);
#6638=ORIENTED_EDGE('',*,*,#5091,.T.);
#6639=ORIENTED_EDGE('',*,*,#5092,.T.);
#6640=ORIENTED_EDGE('',*,*,#5093,.T.);
#6641=ORIENTED_EDGE('',*,*,#5089,.F.);
#6642=ORIENTED_EDGE('',*,*,#5094,.T.);
#6643=ORIENTED_EDGE('',*,*,#5095,.T.);
#6644=ORIENTED_EDGE('',*,*,#5096,.T.);
#6645=ORIENTED_EDGE('',*,*,#5092,.F.);
#6646=ORIENTED_EDGE('',*,*,#5097,.T.);
#6647=ORIENTED_EDGE('',*,*,#5098,.T.);
#6648=ORIENTED_EDGE('',*,*,#5099,.T.);
#6649=ORIENTED_EDGE('',*,*,#5095,.F.);
#6650=ORIENTED_EDGE('',*,*,#5100,.T.);
#6651=ORIENTED_EDGE('',*,*,#5087,.T.);
#6652=ORIENTED_EDGE('',*,*,#5101,.T.);
#6653=ORIENTED_EDGE('',*,*,#5098,.F.);
#6654=ORIENTED_EDGE('',*,*,#5100,.F.);
#6655=ORIENTED_EDGE('',*,*,#5097,.F.);
#6656=ORIENTED_EDGE('',*,*,#5094,.F.);
#6657=ORIENTED_EDGE('',*,*,#5091,.F.);
#6658=ORIENTED_EDGE('',*,*,#5088,.F.);
#6659=ORIENTED_EDGE('',*,*,#5084,.F.);
#6660=ORIENTED_EDGE('',*,*,#5101,.F.);
#6661=ORIENTED_EDGE('',*,*,#5086,.F.);
#6662=ORIENTED_EDGE('',*,*,#5090,.F.);
#6663=ORIENTED_EDGE('',*,*,#5093,.F.);
#6664=ORIENTED_EDGE('',*,*,#5096,.F.);
#6665=ORIENTED_EDGE('',*,*,#5099,.F.);
#7646=CYLINDRICAL_SURFACE('',#9240,0.425);
#7647=CYLINDRICAL_SURFACE('',#9248,0.24505);
#7934=ADVANCED_FACE('',(#1442),#1068,.T.);
#7935=ADVANCED_FACE('',(#1443),#455,.T.);
#7936=ADVANCED_FACE('',(#1444),#7646,.T.);
#7937=ADVANCED_FACE('',(#1445),#456,.T.);
#7938=ADVANCED_FACE('',(#1446,#905),#1069,.T.);
#7939=ADVANCED_FACE('',(#1447),#457,.T.);
#7940=ADVANCED_FACE('',(#1448),#7647,.T.);
#7941=ADVANCED_FACE('',(#1449),#458,.T.);
#7942=ADVANCED_FACE('',(#1450),#1070,.T.);
#7943=ADVANCED_FACE('',(#1451),#1071,.F.);
#7944=ADVANCED_FACE('',(#1452),#1072,.F.);
#7945=ADVANCED_FACE('',(#1453),#1073,.F.);
#7946=ADVANCED_FACE('',(#1454),#1074,.F.);
#7947=ADVANCED_FACE('',(#1455),#1075,.F.);
#7948=ADVANCED_FACE('',(#1456),#1076,.F.);
#7949=ADVANCED_FACE('',(#1457),#1077,.F.);
#7950=ADVANCED_FACE('',(#1458),#1078,.F.);
#8189=CLOSED_SHELL('',(#7934,#7935,#7936,#7937,#7938,#7939,#7940,#7941,
#7942));
#8190=CLOSED_SHELL('',(#7943,#7944,#7945,#7946,#7947,#7948,#7949,#7950));
#9235=AXIS2_PLACEMENT_3D('',#15324,#11055,#11056);
#9236=AXIS2_PLACEMENT_3D('',#15325,#11057,#11058);
#9237=AXIS2_PLACEMENT_3D('',#15327,#11059,#11060);
#9238=AXIS2_PLACEMENT_3D('',#15328,#11061,#11062);
#9239=AXIS2_PLACEMENT_3D('',#15330,#11063,#11064);
#9240=AXIS2_PLACEMENT_3D('',#15332,#11066,#11067);
#9241=AXIS2_PLACEMENT_3D('',#15334,#11068,#11069);
#9242=AXIS2_PLACEMENT_3D('',#15336,#11071,#11072);
#9243=AXIS2_PLACEMENT_3D('',#15338,#11073,#11074);
#9244=AXIS2_PLACEMENT_3D('',#15340,#11076,#11077);
#9245=AXIS2_PLACEMENT_3D('',#15342,#11078,#11079);
#9246=AXIS2_PLACEMENT_3D('',#15343,#11080,#11081);
#9247=AXIS2_PLACEMENT_3D('',#15345,#11082,#11083);
#9248=AXIS2_PLACEMENT_3D('',#15347,#11085,#11086);
#9249=AXIS2_PLACEMENT_3D('',#15349,#11087,#11088);
#9250=AXIS2_PLACEMENT_3D('',#15351,#11090,#11091);
#9251=AXIS2_PLACEMENT_3D('',#15353,#11092,#11093);
#9252=AXIS2_PLACEMENT_3D('',#15355,#11095,#11096);
#9253=AXIS2_PLACEMENT_3D('',#15356,#11097,#11098);
#9254=AXIS2_PLACEMENT_3D('',#15365,#11103,#11104);
#9255=AXIS2_PLACEMENT_3D('',#15371,#11108,#11109);
#9256=AXIS2_PLACEMENT_3D('',#15377,#11113,#11114);
#9257=AXIS2_PLACEMENT_3D('',#15383,#11118,#11119);
#9258=AXIS2_PLACEMENT_3D('',#15389,#11123,#11124);
#9259=AXIS2_PLACEMENT_3D('',#15392,#11127,#11128);
#9260=AXIS2_PLACEMENT_3D('',#15393,#11129,#11130);
#11055=DIRECTION('axis',(0.,0.,1.));
#11056=DIRECTION('refdir',(1.,0.,0.));
#11057=DIRECTION('center_axis',(0.,1.,0.));
#11058=DIRECTION('ref_axis',(0.,0.,1.));
#11059=DIRECTION('center_axis',(0.,-1.,0.));
#11060=DIRECTION('ref_axis',(1.,0.,0.));
#11061=DIRECTION('center_axis',(0.,-1.,0.));
#11062=DIRECTION('ref_axis',(1.,0.,0.));
#11063=DIRECTION('center_axis',(0.,-1.,0.));
#11064=DIRECTION('ref_axis',(1.,0.,0.));
#11065=DIRECTION('',(0.707106781186548,0.707106781186547,8.65956056235493E-17));
#11066=DIRECTION('center_axis',(0.,-1.,0.));
#11067=DIRECTION('ref_axis',(1.,0.,0.));
#11068=DIRECTION('center_axis',(0.,-1.,0.));
#11069=DIRECTION('ref_axis',(1.,0.,0.));
#11070=DIRECTION('',(0.,1.,0.));
#11071=DIRECTION('center_axis',(0.,1.,0.));
#11072=DIRECTION('ref_axis',(1.,0.,0.));
#11073=DIRECTION('center_axis',(0.,-1.,0.));
#11074=DIRECTION('ref_axis',(1.,0.,0.));
#11075=DIRECTION('',(-0.707106781186547,0.707106781186548,-8.65956056235493E-17));
#11076=DIRECTION('center_axis',(0.,-1.,0.));
#11077=DIRECTION('ref_axis',(0.,0.,-1.));
#11078=DIRECTION('center_axis',(0.,-1.,0.));
#11079=DIRECTION('ref_axis',(1.,0.,0.));
#11080=DIRECTION('center_axis',(0.,1.,0.));
#11081=DIRECTION('ref_axis',(1.,0.,0.));
#11082=DIRECTION('center_axis',(0.,1.,0.));
#11083=DIRECTION('ref_axis',(1.,0.,0.));
#11084=DIRECTION('',(-0.447213595499958,0.894427190999916,-5.47678698264203E-17));
#11085=DIRECTION('center_axis',(0.,-1.,0.));
#11086=DIRECTION('ref_axis',(1.,0.,0.));
#11087=DIRECTION('center_axis',(0.,1.,0.));
#11088=DIRECTION('ref_axis',(1.,0.,0.));
#11089=DIRECTION('',(0.,1.,0.));
#11090=DIRECTION('center_axis',(0.,1.,0.));
#11091=DIRECTION('ref_axis',(1.,0.,0.));
#11092=DIRECTION('center_axis',(0.,-1.,0.));
#11093=DIRECTION('ref_axis',(1.,0.,0.));
#11094=DIRECTION('',(-0.707106781186547,0.707106781186548,-8.65956056235493E-17));
#11095=DIRECTION('center_axis',(0.,-1.,0.));
#11096=DIRECTION('ref_axis',(0.,0.,-1.));
#11097=DIRECTION('center_axis',(0.866025403784439,0.,-0.5));
#11098=DIRECTION('ref_axis',(0.5,0.,0.866025403784439));
#11099=DIRECTION('',(-0.5,0.,-0.866025403784439));
#11100=DIRECTION('',(0.,-1.,0.));
#11101=DIRECTION('',(0.5,0.,0.866025403784439));
#11102=DIRECTION('',(0.,-1.,0.));
#11103=DIRECTION('center_axis',(1.20185167898973E-16,0.,-1.));
#11104=DIRECTION('ref_axis',(1.,0.,1.20185167898973E-16));
#11105=DIRECTION('',(-1.,0.,-1.20185167898973E-16));
#11106=DIRECTION('',(0.,-1.,0.));
#11107=DIRECTION('',(1.,0.,1.20185167898973E-16));
#11108=DIRECTION('center_axis',(-0.866025403784439,0.,-0.5));
#11109=DIRECTION('ref_axis',(0.5,0.,-0.866025403784439));
#11110=DIRECTION('',(-0.5,0.,0.866025403784439));
#11111=DIRECTION('',(0.,-1.,0.));
#11112=DIRECTION('',(0.5,0.,-0.866025403784439));
#11113=DIRECTION('center_axis',(-0.866025403784439,0.,0.5));
#11114=DIRECTION('ref_axis',(-0.5,0.,-0.866025403784439));
#11115=DIRECTION('',(0.5,0.,0.866025403784439));
#11116=DIRECTION('',(0.,-1.,0.));
#11117=DIRECTION('',(-0.5,0.,-0.866025403784439));
#11118=DIRECTION('center_axis',(-2.40370335797945E-16,0.,1.));
#11119=DIRECTION('ref_axis',(-1.,0.,-2.40370335797945E-16));
#11120=DIRECTION('',(1.,0.,2.40370335797945E-16));
#11121=DIRECTION('',(0.,-1.,0.));
#11122=DIRECTION('',(-1.,0.,-2.40370335797945E-16));
#11123=DIRECTION('center_axis',(0.866025403784439,0.,0.5));
#11124=DIRECTION('ref_axis',(-0.5,0.,0.866025403784439));
#11125=DIRECTION('',(0.5,0.,-0.866025403784439));
#11126=DIRECTION('',(-0.5,0.,0.866025403784439));
#11127=DIRECTION('center_axis',(0.,1.,0.));
#11128=DIRECTION('ref_axis',(1.,0.,0.));
#11129=DIRECTION('center_axis',(0.,-1.,0.));
#11130=DIRECTION('ref_axis',(0.,0.,-1.));
#15324=CARTESIAN_POINT('',(0.,0.,0.));
#15325=CARTESIAN_POINT('Origin',(0.375,0.5,0.));
#15326=CARTESIAN_POINT('',(-0.375,0.5,-4.59242549680257E-17));
#15327=CARTESIAN_POINT('Origin',(0.,0.5,0.));
#15328=CARTESIAN_POINT('Origin',(0.,0.475,0.));
#15329=CARTESIAN_POINT('',(-0.425,0.45,-5.20474889637625E-17));
#15330=CARTESIAN_POINT('Origin',(0.,0.45,0.));
#15331=CARTESIAN_POINT('',(-0.4,0.475,-4.89858719658941E-17));
#15332=CARTESIAN_POINT('Origin',(0.,0.24,0.));
#15333=CARTESIAN_POINT('',(-0.425,0.0299999999999998,-5.20474889637625E-17));
#15334=CARTESIAN_POINT('Origin',(0.,0.0299999999999998,0.));
#15335=CARTESIAN_POINT('',(-0.425,0.24,-5.20474889637625E-17));
#15336=CARTESIAN_POINT('Origin',(0.,0.0150000000000001,0.));
#15337=CARTESIAN_POINT('',(-0.395,4.85722573273506E-17,-4.83735485663204E-17));
#15338=CARTESIAN_POINT('Origin',(0.,0.,0.));
#15339=CARTESIAN_POINT('',(-0.41,0.0150000000000001,-5.02105187650415E-17));
#15340=CARTESIAN_POINT('Origin',(0.27,0.,0.));
#15341=CARTESIAN_POINT('',(-0.27,0.,-3.30654635769785E-17));
#15342=CARTESIAN_POINT('Origin',(0.,0.,0.));
#15343=CARTESIAN_POINT('Origin',(0.,-0.02,0.));
#15344=CARTESIAN_POINT('',(-0.24505,-0.0498999999999999,3.00099698131059E-17));
#15345=CARTESIAN_POINT('Origin',(0.,-0.0498999999999999,0.));
#15346=CARTESIAN_POINT('',(-0.26,-0.02,-3.18408167778312E-17));
#15347=CARTESIAN_POINT('Origin',(0.,-0.995,0.));
#15348=CARTESIAN_POINT('',(-0.24505,-1.95495,3.00099698131059E-17));
#15349=CARTESIAN_POINT('Origin',(0.,-1.95495,0.));
#15350=CARTESIAN_POINT('',(-0.24505,-0.995,-3.00099698131059E-17));
#15351=CARTESIAN_POINT('Origin',(0.,-1.975,0.));
#15352=CARTESIAN_POINT('',(-0.2,-2.,-2.44929359829471E-17));
#15353=CARTESIAN_POINT('Origin',(0.,-2.,0.));
#15354=CARTESIAN_POINT('',(-0.225,-1.975,-2.75545529808154E-17));
#15355=CARTESIAN_POINT('Origin',(0.,-2.,0.));
#15356=CARTESIAN_POINT('Origin',(0.115470053837925,-0.5,-0.2));
#15357=CARTESIAN_POINT('',(0.23094010767585,-0.5,0.));
#15358=CARTESIAN_POINT('',(0.115470053837925,-0.5,-0.2));
#15359=CARTESIAN_POINT('',(0.23094010767585,-0.5,0.));
#15360=CARTESIAN_POINT('',(0.115470053837925,-0.8,-0.2));
#15361=CARTESIAN_POINT('',(0.115470053837925,-0.5,-0.2));
#15362=CARTESIAN_POINT('',(0.23094010767585,-0.8,0.));
#15363=CARTESIAN_POINT('',(0.23094010767585,-0.8,0.));
#15364=CARTESIAN_POINT('',(0.23094010767585,-0.5,0.));
#15365=CARTESIAN_POINT('Origin',(-0.115470053837925,-0.5,-0.2));
#15366=CARTESIAN_POINT('',(-0.115470053837925,-0.5,-0.2));
#15367=CARTESIAN_POINT('',(0.115470053837925,-0.5,-0.2));
#15368=CARTESIAN_POINT('',(-0.115470053837925,-0.8,-0.2));
#15369=CARTESIAN_POINT('',(-0.115470053837925,-0.5,-0.2));
#15370=CARTESIAN_POINT('',(0.115470053837925,-0.8,-0.2));
#15371=CARTESIAN_POINT('Origin',(-0.23094010767585,-0.5,-2.77555756156289E-17));
#15372=CARTESIAN_POINT('',(-0.23094010767585,-0.5,-2.82820063659975E-17));
#15373=CARTESIAN_POINT('',(-0.115470053837925,-0.5,-0.2));
#15374=CARTESIAN_POINT('',(-0.23094010767585,-0.8,-2.77555756156289E-17));
#15375=CARTESIAN_POINT('',(-0.23094010767585,-0.5,-2.82820063659975E-17));
#15376=CARTESIAN_POINT('',(-0.115470053837925,-0.8,-0.2));
#15377=CARTESIAN_POINT('Origin',(-0.115470053837925,-0.5,0.2));
#15378=CARTESIAN_POINT('',(-0.115470053837925,-0.5,0.2));
#15379=CARTESIAN_POINT('',(-0.23094010767585,-0.5,-2.82820063659975E-17));
#15380=CARTESIAN_POINT('',(-0.115470053837925,-0.8,0.2));
#15381=CARTESIAN_POINT('',(-0.115470053837925,-0.5,0.2));
#15382=CARTESIAN_POINT('',(-0.23094010767585,-0.8,-2.82820063659975E-17));
#15383=CARTESIAN_POINT('Origin',(0.115470053837925,-0.5,0.2));
#15384=CARTESIAN_POINT('',(0.115470053837925,-0.5,0.2));
#15385=CARTESIAN_POINT('',(-0.115470053837925,-0.5,0.2));
#15386=CARTESIAN_POINT('',(0.115470053837925,-0.8,0.2));
#15387=CARTESIAN_POINT('',(0.115470053837925,-0.5,0.2));
#15388=CARTESIAN_POINT('',(-0.115470053837925,-0.8,0.2));
#15389=CARTESIAN_POINT('Origin',(0.23094010767585,-0.5,0.));
#15390=CARTESIAN_POINT('',(0.115470053837925,-0.5,0.2));
#15391=CARTESIAN_POINT('',(0.115470053837925,-0.8,0.2));
#15392=CARTESIAN_POINT('Origin',(0.,-0.5,0.));
#15393=CARTESIAN_POINT('Origin',(0.,-0.8,0.));
#16966=UNCERTAINTY_MEASURE_WITH_UNIT(LENGTH_MEASURE(0.001),#17047,
'DISTANCE_ACCURACY_VALUE',
'Maximum model space distance between geometric entities at asserted c
onnectivities');
#16993=UNCERTAINTY_MEASURE_WITH_UNIT(LENGTH_MEASURE(0.001),#17047,
'DISTANCE_ACCURACY_VALUE',
'Maximum model space distance between geometric entities at asserted c
onnectivities');
#17019=(
GEOMETRIC_REPRESENTATION_CONTEXT(3)
GLOBAL_UNCERTAINTY_ASSIGNED_CONTEXT((#16966))
GLOBAL_UNIT_ASSIGNED_CONTEXT((#17047,#17049,#17050))
REPRESENTATION_CONTEXT('','3D')
);
#17046=(
GEOMETRIC_REPRESENTATION_CONTEXT(3)
GLOBAL_UNCERTAINTY_ASSIGNED_CONTEXT((#16993))
GLOBAL_UNIT_ASSIGNED_CONTEXT((#17047,#17049,#17050))
REPRESENTATION_CONTEXT('','3D')
);
#17047=(
LENGTH_UNIT()
NAMED_UNIT(*)
SI_UNIT(.CENTI.,.METRE.)
);
#17049=(
NAMED_UNIT(*)
PLANE_ANGLE_UNIT()
SI_UNIT($,.RADIAN.)
);
#17050=(
NAMED_UNIT(*)
SI_UNIT($,.STERADIAN.)
SOLID_ANGLE_UNIT()
);
#17076=SHAPE_DEFINITION_REPRESENTATION(#17128,#17283);
#17128=PRODUCT_DEFINITION_SHAPE('',$,#17336);
#17283=SHAPE_REPRESENTATION('',(#9235),#17019);
#17310=PRODUCT_DEFINITION_CONTEXT('part definition',#17468,'design');
#17336=PRODUCT_DEFINITION('Cap Screw - M5x20','Cap Screw - M5x20',#17388,
#17310);
#17388=PRODUCT_DEFINITION_FORMATION('',$,#17495);
#17468=APPLICATION_CONTEXT(
'Core Data for Automotive Mechanical Design Process');
#17469=PRODUCT_CONTEXT('part definition',#17468,'mechanical');
#17495=PRODUCT('Cap Screw - M5x20','Cap Screw - M5x20',
'Cap Screw - M5x20',(#17469));
#17592=COLOUR_RGB('Black',0.12,0.14,0.17);
#17593=FILL_AREA_STYLE_COLOUR('',#17592);
#17594=FILL_AREA_STYLE('',(#17593));
#17595=SURFACE_STYLE_FILL_AREA(#17594);
#17596=SURFACE_SIDE_STYLE('',(#17595));
#17597=SURFACE_STYLE_USAGE(.BOTH.,#17596);
#17598=PRESENTATION_STYLE_ASSIGNMENT((#17597));
ENDSEC;
END-ISO-10303-21;
